ISO-10303-21;
HEADER;
/* Generated by software containing ST-Developer
 * from STEP Tools, Inc. (www.steptools.com) 
 */

FILE_DESCRIPTION(
/* description */ (''),
/* implementation_level */ '2;1');

FILE_NAME(
/* name */ '12_ISO_7089_Washer_8.step',
/* time_stamp */ '2026-10-11T08:27:52-07:00',
/* author */ (''),
/* organization */ (''),
/* preprocessor_version */ 'ST-DEVELOPER v20.2',
/* originating_system */ 'Autodesk Translation Framework v15.15.0.0',
/* authorisation */ '');

FILE_SCHEMA (('AUTOMOTIVE_DESIGN { 1 0 10303 214 3 1 1 }'));
ENDSEC;

DATA;
#10=MECHANICAL_DESIGN_GEOMETRIC_PRESENTATION_REPRESENTATION('',(#930),#94301);
#902=SHAPE_REPRESENTATION_RELATIONSHIP('SRR','None',#94382,#916);
#916=ADVANCED_BREP_SHAPE_REPRESENTATION('',(#944),#94298);
#930=STYLED_ITEM('',(#94588),#944);
#944=MANIFOLD_SOLID_BREP('Body1',#51029);
#1040=FACE_BOUND('',#18666,.T.);
#1041=FACE_BOUND('',#18671,.T.);
#1282=CYLINDRICAL_SURFACE('',#55275,8.);
#1283=CYLINDRICAL_SURFACE('',#55283,4.2);
#6666=LINE('',#94052,#11194);
#6667=LINE('',#94057,#11195);
#6668=LINE('',#94061,#11196);
#6669=LINE('',#94067,#11197);
#6670=LINE('',#94071,#11198);
#6671=LINE('',#94075,#11199);
#11194=VECTOR('',#68048,7.9);
#11195=VECTOR('',#68055,8.);
#11196=VECTOR('',#68060,7.9);
#11197=VECTOR('',#68067,4.3);
#11198=VECTOR('',#68072,4.2);
#11199=VECTOR('',#68077,4.3);
#13235=PLANE('',#55279);
#13236=PLANE('',#55287);
#15899=FACE_OUTER_BOUND('',#18662,.T.);
#15900=FACE_OUTER_BOUND('',#18663,.T.);
#15901=FACE_OUTER_BOUND('',#18664,.T.);
#15902=FACE_OUTER_BOUND('',#18665,.T.);
#15903=FACE_OUTER_BOUND('',#18667,.T.);
#15904=FACE_OUTER_BOUND('',#18668,.T.);
#15905=FACE_OUTER_BOUND('',#18669,.T.);
#15906=FACE_OUTER_BOUND('',#18670,.T.);
#18662=EDGE_LOOP('',(#47975,#47976,#47977,#47978));
#18663=EDGE_LOOP('',(#47979,#47980,#47981,#47982));
#18664=EDGE_LOOP('',(#47983,#47984,#47985,#47986));
#18665=EDGE_LOOP('',(#47987));
#18666=EDGE_LOOP('',(#47988));
#18667=EDGE_LOOP('',(#47989,#47990,#47991,#47992));
#18668=EDGE_LOOP('',(#47993,#47994,#47995,#47996));
#18669=EDGE_LOOP('',(#47997,#47998,#47999,#48000));
#18670=EDGE_LOOP('',(#48001));
#18671=EDGE_LOOP('',(#48002));
#20300=CIRCLE('',#55273,8.);
#20301=CIRCLE('',#55274,7.8);
#20302=CIRCLE('',#55276,8.);
#20303=CIRCLE('',#55278,7.8);
#20304=CIRCLE('',#55280,4.4);
#20305=CIRCLE('',#55282,4.2);
#20306=CIRCLE('',#55284,4.2);
#20307=CIRCLE('',#55286,4.4);
#25277=VERTEX_POINT('',#94049);
#25278=VERTEX_POINT('',#94051);
#25279=VERTEX_POINT('',#94055);
#25280=VERTEX_POINT('',#94059);
#25281=VERTEX_POINT('',#94063);
#25282=VERTEX_POINT('',#94066);
#25283=VERTEX_POINT('',#94070);
#25284=VERTEX_POINT('',#94074);
#32849=EDGE_CURVE('',#25277,#25277,#20300,.T.);
#32850=EDGE_CURVE('',#25277,#25278,#6666,.T.);
#32851=EDGE_CURVE('',#25278,#25278,#20301,.T.);
#32852=EDGE_CURVE('',#25279,#25279,#20302,.T.);
#32853=EDGE_CURVE('',#25279,#25277,#6667,.T.);
#32854=EDGE_CURVE('',#25280,#25280,#20303,.T.);
#32855=EDGE_CURVE('',#25280,#25279,#6668,.T.);
#32856=EDGE_CURVE('',#25281,#25281,#20304,.T.);
#32857=EDGE_CURVE('',#25281,#25282,#6669,.T.);
#32858=EDGE_CURVE('',#25282,#25282,#20305,.T.);
#32859=EDGE_CURVE('',#25282,#25283,#6670,.T.);
#32860=EDGE_CURVE('',#25283,#25283,#20306,.T.);
#32861=EDGE_CURVE('',#25283,#25284,#6671,.T.);
#32862=EDGE_CURVE('',#25284,#25284,#20307,.T.);
#47975=ORIENTED_EDGE('',*,*,#32849,.F.);
#47976=ORIENTED_EDGE('',*,*,#32850,.T.);
#47977=ORIENTED_EDGE('',*,*,#32851,.T.);
#47978=ORIENTED_EDGE('',*,*,#32850,.F.);
#47979=ORIENTED_EDGE('',*,*,#32852,.F.);
#47980=ORIENTED_EDGE('',*,*,#32853,.T.);
#47981=ORIENTED_EDGE('',*,*,#32849,.T.);
#47982=ORIENTED_EDGE('',*,*,#32853,.F.);
#47983=ORIENTED_EDGE('',*,*,#32854,.F.);
#47984=ORIENTED_EDGE('',*,*,#32855,.T.);
#47985=ORIENTED_EDGE('',*,*,#32852,.T.);
#47986=ORIENTED_EDGE('',*,*,#32855,.F.);
#47987=ORIENTED_EDGE('',*,*,#32854,.T.);
#47988=ORIENTED_EDGE('',*,*,#32856,.F.);
#47989=ORIENTED_EDGE('',*,*,#32856,.T.);
#47990=ORIENTED_EDGE('',*,*,#32857,.T.);
#47991=ORIENTED_EDGE('',*,*,#32858,.F.);
#47992=ORIENTED_EDGE('',*,*,#32857,.F.);
#47993=ORIENTED_EDGE('',*,*,#32858,.T.);
#47994=ORIENTED_EDGE('',*,*,#32859,.T.);
#47995=ORIENTED_EDGE('',*,*,#32860,.F.);
#47996=ORIENTED_EDGE('',*,*,#32859,.F.);
#47997=ORIENTED_EDGE('',*,*,#32860,.T.);
#47998=ORIENTED_EDGE('',*,*,#32861,.T.);
#47999=ORIENTED_EDGE('',*,*,#32862,.F.);
#48000=ORIENTED_EDGE('',*,*,#32861,.F.);
#48001=ORIENTED_EDGE('',*,*,#32851,.F.);
#48002=ORIENTED_EDGE('',*,*,#32862,.T.);
#48324=CONICAL_SURFACE('',#55272,7.9,0.785398163397449);
#48325=CONICAL_SURFACE('',#55277,7.9,0.785398163397449);
#48326=CONICAL_SURFACE('',#55281,4.3,0.785398163397449);
#48327=CONICAL_SURFACE('',#55285,4.3,0.785398163397449);
#50986=ADVANCED_FACE('',(#15899),#48324,.T.);
#50987=ADVANCED_FACE('',(#15900),#1282,.T.);
#50988=ADVANCED_FACE('',(#15901),#48325,.T.);
#50989=ADVANCED_FACE('',(#15902,#1040),#13235,.T.);
#50990=ADVANCED_FACE('',(#15903),#48326,.F.);
#50991=ADVANCED_FACE('',(#15904),#1283,.F.);
#50992=ADVANCED_FACE('',(#15905),#48327,.F.);
#50993=ADVANCED_FACE('',(#15906,#1041),#13236,.T.);
#51029=CLOSED_SHELL('',(#50986,#50987,#50988,#50989,#50990,#50991,#50992,
#50993));
#55271=AXIS2_PLACEMENT_3D('',#94047,#68042,#68043);
#55272=AXIS2_PLACEMENT_3D('',#94048,#68044,#68045);
#55273=AXIS2_PLACEMENT_3D('',#94050,#68046,#68047);
#55274=AXIS2_PLACEMENT_3D('',#94053,#68049,#68050);
#55275=AXIS2_PLACEMENT_3D('',#94054,#68051,#68052);
#55276=AXIS2_PLACEMENT_3D('',#94056,#68053,#68054);
#55277=AXIS2_PLACEMENT_3D('',#94058,#68056,#68057);
#55278=AXIS2_PLACEMENT_3D('',#94060,#68058,#68059);
#55279=AXIS2_PLACEMENT_3D('',#94062,#68061,#68062);
#55280=AXIS2_PLACEMENT_3D('',#94064,#68063,#68064);
#55281=AXIS2_PLACEMENT_3D('',#94065,#68065,#68066);
#55282=AXIS2_PLACEMENT_3D('',#94068,#68068,#68069);
#55283=AXIS2_PLACEMENT_3D('',#94069,#68070,#68071);
#55284=AXIS2_PLACEMENT_3D('',#94072,#68073,#68074);
#55285=AXIS2_PLACEMENT_3D('',#94073,#68075,#68076);
#55286=AXIS2_PLACEMENT_3D('',#94076,#68078,#68079);
#55287=AXIS2_PLACEMENT_3D('',#94077,#68080,#68081);
#68042=DIRECTION('axis',(0.,0.,1.));
#68043=DIRECTION('refdir',(1.,0.,0.));
#68044=DIRECTION('center_axis',(1.,0.,0.));
#68045=DIRECTION('ref_axis',(0.,1.,0.));
#68046=DIRECTION('center_axis',(1.,0.,0.));
#68047=DIRECTION('ref_axis',(0.,0.,-1.));
#68048=DIRECTION('',(-0.707106781186547,0.707106781186548,8.65956056235494E-17));
#68049=DIRECTION('center_axis',(1.,0.,0.));
#68050=DIRECTION('ref_axis',(0.,0.,-1.));
#68051=DIRECTION('center_axis',(1.,0.,0.));
#68052=DIRECTION('ref_axis',(0.,1.,0.));
#68053=DIRECTION('center_axis',(1.,0.,0.));
#68054=DIRECTION('ref_axis',(0.,0.,-1.));
#68055=DIRECTION('',(-1.,0.,0.));
#68056=DIRECTION('center_axis',(-1.,0.,0.));
#68057=DIRECTION('ref_axis',(0.,1.,0.));
#68058=DIRECTION('center_axis',(1.,0.,0.));
#68059=DIRECTION('ref_axis',(0.,0.,-1.));
#68060=DIRECTION('',(-0.707106781186547,-0.707106781186548,-8.65956056235494E-17));
#68061=DIRECTION('center_axis',(1.,0.,0.));
#68062=DIRECTION('ref_axis',(0.,0.,-1.));
#68063=DIRECTION('center_axis',(1.,0.,0.));
#68064=DIRECTION('ref_axis',(0.,0.,-1.));
#68065=DIRECTION('center_axis',(1.,0.,0.));
#68066=DIRECTION('ref_axis',(0.,1.,0.));
#68067=DIRECTION('',(-0.707106781186547,0.707106781186548,8.65956056235494E-17));
#68068=DIRECTION('center_axis',(1.,0.,0.));
#68069=DIRECTION('ref_axis',(0.,0.,-1.));
#68070=DIRECTION('center_axis',(1.,0.,0.));
#68071=DIRECTION('ref_axis',(0.,1.,0.));
#68072=DIRECTION('',(-1.,0.,0.));
#68073=DIRECTION('center_axis',(1.,0.,0.));
#68074=DIRECTION('ref_axis',(0.,0.,-1.));
#68075=DIRECTION('center_axis',(-1.,0.,0.));
#68076=DIRECTION('ref_axis',(0.,1.,0.));
#68077=DIRECTION('',(-0.707106781186547,-0.707106781186548,-8.65956056235494E-17));
#68078=DIRECTION('center_axis',(1.,0.,0.));
#68079=DIRECTION('ref_axis',(0.,0.,-1.));
#68080=DIRECTION('center_axis',(-1.,0.,0.));
#68081=DIRECTION('ref_axis',(0.,0.,1.));
#94047=CARTESIAN_POINT('',(0.,0.,0.));
#94048=CARTESIAN_POINT('Origin',(0.1,0.,0.));
#94049=CARTESIAN_POINT('',(0.2,-8.,-9.79717439317883E-16));
#94050=CARTESIAN_POINT('Origin',(0.2,0.,0.));
#94051=CARTESIAN_POINT('',(-1.21430643318376E-16,-7.8,-9.55224503334936E-16));
#94052=CARTESIAN_POINT('',(0.1,-7.9,-9.67470971326409E-16));
#94053=CARTESIAN_POINT('Origin',(0.,0.,0.));
#94054=CARTESIAN_POINT('Origin',(0.8,0.,0.));
#94055=CARTESIAN_POINT('',(1.4,-8.,-9.79717439317883E-16));
#94056=CARTESIAN_POINT('Origin',(1.4,0.,0.));
#94057=CARTESIAN_POINT('',(0.8,-8.,-9.79717439317883E-16));
#94058=CARTESIAN_POINT('Origin',(1.5,0.,0.));
#94059=CARTESIAN_POINT('',(1.6,-7.8,-9.55224503334936E-16));
#94060=CARTESIAN_POINT('Origin',(1.6,0.,0.));
#94061=CARTESIAN_POINT('',(1.5,-7.9,-9.67470971326409E-16));
#94062=CARTESIAN_POINT('Origin',(1.6,4.4,0.));
#94063=CARTESIAN_POINT('',(1.6,-4.4,-5.38844591624835E-16));
#94064=CARTESIAN_POINT('Origin',(1.6,0.,0.));
#94065=CARTESIAN_POINT('Origin',(1.5,0.,0.));
#94066=CARTESIAN_POINT('',(1.4,-4.2,-5.14351655641888E-16));
#94067=CARTESIAN_POINT('',(1.5,-4.3,-5.26598123633362E-16));
#94068=CARTESIAN_POINT('Origin',(1.4,0.,0.));
#94069=CARTESIAN_POINT('Origin',(0.8,0.,0.));
#94070=CARTESIAN_POINT('',(0.2,-4.2,-5.14351655641888E-16));
#94071=CARTESIAN_POINT('',(0.8,-4.2,-5.14351655641888E-16));
#94072=CARTESIAN_POINT('Origin',(0.2,0.,0.));
#94073=CARTESIAN_POINT('Origin',(0.1,0.,0.));
#94074=CARTESIAN_POINT('',(-5.20417042793042E-17,-4.4,-5.38844591624835E-16));
#94075=CARTESIAN_POINT('',(0.1,-4.3,-5.26598123633362E-16));
#94076=CARTESIAN_POINT('Origin',(0.,0.,0.));
#94077=CARTESIAN_POINT('Origin',(0.,7.8,0.));
#94282=UNCERTAINTY_MEASURE_WITH_UNIT(LENGTH_MEASURE(0.01),#94302,
'DISTANCE_ACCURACY_VALUE',
'Maximum model space distance between geometric entities at asserted c
onnectivities');
#94285=UNCERTAINTY_MEASURE_WITH_UNIT(LENGTH_MEASURE(0.01),#94302,
'DISTANCE_ACCURACY_VALUE',
'Maximum model space distance between geometric entities at asserted c
onnectivities');
#94298=(
GEOMETRIC_REPRESENTATION_CONTEXT(3)
GLOBAL_UNCERTAINTY_ASSIGNED_CONTEXT((#94282))
GLOBAL_UNIT_ASSIGNED_CONTEXT((#94302,#94304,#94305))
REPRESENTATION_CONTEXT('','3D')
);
#94301=(
GEOMETRIC_REPRESENTATION_CONTEXT(3)
GLOBAL_UNCERTAINTY_ASSIGNED_CONTEXT((#94285))
GLOBAL_UNIT_ASSIGNED_CONTEXT((#94302,#94304,#94305))
REPRESENTATION_CONTEXT('','3D')
);
#94302=(
LENGTH_UNIT()
NAMED_UNIT(*)
SI_UNIT(.MILLI.,.METRE.)
);
#94304=(
NAMED_UNIT(*)
PLANE_ANGLE_UNIT()
SI_UNIT($,.RADIAN.)
);
#94305=(
NAMED_UNIT(*)
SI_UNIT($,.STERADIAN.)
SOLID_ANGLE_UNIT()
);
#94318=SHAPE_DEFINITION_REPRESENTATION(#94333,#94382);
#94333=PRODUCT_DEFINITION_SHAPE('',$,#94398);
#94382=SHAPE_REPRESENTATION('',(#55271),#94298);
#94385=PRODUCT_DEFINITION_CONTEXT('part definition',#94432,'design');
#94398=PRODUCT_DEFINITION('2026-10-11-08-26-48-006',
'12_ISO_7089_Washer_8',#94413,#94385);
#94413=PRODUCT_DEFINITION_FORMATION('',$,#94446);
#94432=APPLICATION_CONTEXT(
'Core Data for Automotive Mechanical Design Process');
#94433=PRODUCT_CONTEXT('part definition',#94432,'mechanical');
#94446=PRODUCT('2026-10-11-08-26-48-006','12_ISO_7089_Washer_8',$,(#94433));
#94582=COLOUR_RGB('Black',0.12,0.14,0.17);
#94583=FILL_AREA_STYLE_COLOUR('',#94582);
#94584=FILL_AREA_STYLE('',(#94583));
#94585=SURFACE_STYLE_FILL_AREA(#94584);
#94586=SURFACE_SIDE_STYLE('',(#94585));
#94587=SURFACE_STYLE_USAGE(.BOTH.,#94586);
#94588=PRESENTATION_STYLE_ASSIGNMENT((#94587));
ENDSEC;
END-ISO-10303-21;
